ISO-10303-21;
HEADER;
/* Generated by software containing ST-Developer
 * from STEP Tools, Inc. (www.steptools.com) 
 */

FILE_DESCRIPTION(
/* description */ ('XY cross-slide table'),
/* implementation_level */ '2;1');

FILE_NAME(
/* name */ 'Flat Washer - M6.step',
/* time_stamp */ '2026-10-28T03:22:46-07:00',
/* author */ (''),
/* organization */ (''),
/* preprocessor_version */ 'ST-DEVELOPER v20.2',
/* originating_system */ 'Autodesk Translation Framework v15.17.0.0',
/* authorisation */ '');

FILE_SCHEMA (('AUTOMOTIVE_DESIGN { 1 0 10303 214 3 1 1 }'));
ENDSEC;

DATA;
#10=MECHANICAL_DESIGN_GEOMETRIC_PRESENTATION_REPRESENTATION('',(#1725),#62984);
#1544=SHAPE_REPRESENTATION_RELATIONSHIP('SRR','None',#63397,#1627);
#1627=ADVANCED_BREP_SHAPE_REPRESENTATION('',(#1835),#62934);
#1725=STYLED_ITEM('',(#63919),#1835);
#1835=MANIFOLD_SOLID_BREP('Body1',#23022);
#2082=FACE_BOUND('',#5003,.T.);
#2083=FACE_BOUND('',#5005,.T.);
#2564=PLANE('',#25125);
#2565=PLANE('',#25126);
#3491=FACE_OUTER_BOUND('',#5000,.T.);
#3492=FACE_OUTER_BOUND('',#5001,.T.);
#3493=FACE_OUTER_BOUND('',#5002,.T.);
#3494=FACE_OUTER_BOUND('',#5004,.T.);
#5000=EDGE_LOOP('',(#17854,#17855,#17856,#17857));
#5001=EDGE_LOOP('',(#17858,#17859,#17860,#17861));
#5002=EDGE_LOOP('',(#17862));
#5003=EDGE_LOOP('',(#17863));
#5004=EDGE_LOOP('',(#17864));
#5005=EDGE_LOOP('',(#17865));
#6618=LINE('',#47652,#8105);
#6619=LINE('',#47658,#8106);
#8105=VECTOR('',#29415,0.32);
#8106=VECTOR('',#29422,0.6);
#9299=CIRCLE('',#25120,0.32);
#9300=CIRCLE('',#25121,0.32);
#9301=CIRCLE('',#25123,0.6);
#9302=CIRCLE('',#25124,0.6);
#10767=VERTEX_POINT('',#47649);
#10768=VERTEX_POINT('',#47651);
#10769=VERTEX_POINT('',#47655);
#10770=VERTEX_POINT('',#47657);
#13311=EDGE_CURVE('',#10767,#10767,#9299,.T.);
#13312=EDGE_CURVE('',#10767,#10768,#6618,.T.);
#13313=EDGE_CURVE('',#10768,#10768,#9300,.T.);
#13314=EDGE_CURVE('',#10769,#10769,#9301,.T.);
#13315=EDGE_CURVE('',#10769,#10770,#6619,.T.);
#13316=EDGE_CURVE('',#10770,#10770,#9302,.T.);
#17854=ORIENTED_EDGE('',*,*,#13311,.F.);
#17855=ORIENTED_EDGE('',*,*,#13312,.T.);
#17856=ORIENTED_EDGE('',*,*,#13313,.T.);
#17857=ORIENTED_EDGE('',*,*,#13312,.F.);
#17858=ORIENTED_EDGE('',*,*,#13314,.F.);
#17859=ORIENTED_EDGE('',*,*,#13315,.T.);
#17860=ORIENTED_EDGE('',*,*,#13316,.T.);
#17861=ORIENTED_EDGE('',*,*,#13315,.F.);
#17862=ORIENTED_EDGE('',*,*,#13314,.T.);
#17863=ORIENTED_EDGE('',*,*,#13311,.T.);
#17864=ORIENTED_EDGE('',*,*,#13316,.F.);
#17865=ORIENTED_EDGE('',*,*,#13313,.F.);
#21334=CYLINDRICAL_SURFACE('',#25119,0.32);
#21335=CYLINDRICAL_SURFACE('',#25122,0.6);
#22272=ADVANCED_FACE('',(#3491),#21334,.F.);
#22273=ADVANCED_FACE('',(#3492),#21335,.T.);
#22274=ADVANCED_FACE('',(#3493,#2082),#2564,.T.);
#22275=ADVANCED_FACE('',(#3494,#2083),#2565,.F.);
#23022=CLOSED_SHELL('',(#22272,#22273,#22274,#22275));
#25118=AXIS2_PLACEMENT_3D('',#47647,#29409,#29410);
#25119=AXIS2_PLACEMENT_3D('',#47648,#29411,#29412);
#25120=AXIS2_PLACEMENT_3D('',#47650,#29413,#29414);
#25121=AXIS2_PLACEMENT_3D('',#47653,#29416,#29417);
#25122=AXIS2_PLACEMENT_3D('',#47654,#29418,#29419);
#25123=AXIS2_PLACEMENT_3D('',#47656,#29420,#29421);
#25124=AXIS2_PLACEMENT_3D('',#47659,#29423,#29424);
#25125=AXIS2_PLACEMENT_3D('',#47660,#29425,#29426);
#25126=AXIS2_PLACEMENT_3D('',#47661,#29427,#29428);
#29409=DIRECTION('axis',(0.,0.,1.));
#29410=DIRECTION('refdir',(1.,0.,0.));
#29411=DIRECTION('center_axis',(0.,1.,0.));
#29412=DIRECTION('ref_axis',(1.,0.,0.));
#29413=DIRECTION('center_axis',(0.,-1.,0.));
#29414=DIRECTION('ref_axis',(1.,0.,0.));
#29415=DIRECTION('',(0.,-1.,0.));
#29416=DIRECTION('center_axis',(0.,-1.,0.));
#29417=DIRECTION('ref_axis',(1.,0.,0.));
#29418=DIRECTION('center_axis',(0.,1.,0.));
#29419=DIRECTION('ref_axis',(1.,0.,0.));
#29420=DIRECTION('center_axis',(0.,1.,0.));
#29421=DIRECTION('ref_axis',(1.,0.,0.));
#29422=DIRECTION('',(0.,-1.,0.));
#29423=DIRECTION('center_axis',(0.,1.,0.));
#29424=DIRECTION('ref_axis',(1.,0.,0.));
#29425=DIRECTION('center_axis',(0.,1.,0.));
#29426=DIRECTION('ref_axis',(1.,0.,0.));
#29427=DIRECTION('center_axis',(0.,1.,0.));
#29428=DIRECTION('ref_axis',(1.,0.,0.));
#47647=CARTESIAN_POINT('',(0.,0.,0.));
#47648=CARTESIAN_POINT('Origin',(0.,0.,0.));
#47649=CARTESIAN_POINT('',(-0.32,0.16,3.91886975727153E-17));
#47650=CARTESIAN_POINT('Origin',(0.,0.16,0.));
#47651=CARTESIAN_POINT('',(-0.32,0.,3.91886975727153E-17));
#47652=CARTESIAN_POINT('',(-0.32,0.,3.91886975727153E-17));
#47653=CARTESIAN_POINT('Origin',(0.,0.,0.));
#47654=CARTESIAN_POINT('Origin',(0.,0.,0.));
#47655=CARTESIAN_POINT('',(-0.6,0.16,7.34788079488412E-17));
#47656=CARTESIAN_POINT('Origin',(0.,0.16,0.));
#47657=CARTESIAN_POINT('',(-0.6,0.,7.34788079488412E-17));
#47658=CARTESIAN_POINT('',(-0.6,0.,7.34788079488412E-17));
#47659=CARTESIAN_POINT('Origin',(0.,0.,0.));
#47660=CARTESIAN_POINT('Origin',(0.,0.16,0.));
#47661=CARTESIAN_POINT('Origin',(0.,0.,0.));
#62835=UNCERTAINTY_MEASURE_WITH_UNIT(LENGTH_MEASURE(0.001),#62985,
'DISTANCE_ACCURACY_VALUE',
'Maximum model space distance between geometric entities at asserted c
onnectivities');
#62885=UNCERTAINTY_MEASURE_WITH_UNIT(LENGTH_MEASURE(0.001),#62985,
'DISTANCE_ACCURACY_VALUE',
'Maximum model space distance between geometric entities at asserted c
onnectivities');
#62934=(
GEOMETRIC_REPRESENTATION_CONTEXT(3)
GLOBAL_UNCERTAINTY_ASSIGNED_CONTEXT((#62835))
GLOBAL_UNIT_ASSIGNED_CONTEXT((#62985,#62987,#62988))
REPRESENTATION_CONTEXT('','3D')
);
#62984=(
GEOMETRIC_REPRESENTATION_CONTEXT(3)
GLOBAL_UNCERTAINTY_ASSIGNED_CONTEXT((#62885))
GLOBAL_UNIT_ASSIGNED_CONTEXT((#62985,#62987,#62988))
REPRESENTATION_CONTEXT('','3D')
);
#62985=(
LENGTH_UNIT()
NAMED_UNIT(*)
SI_UNIT(.CENTI.,.METRE.)
);
#62987=(
NAMED_UNIT(*)
PLANE_ANGLE_UNIT()
SI_UNIT($,.RADIAN.)
);
#62988=(
NAMED_UNIT(*)
SI_UNIT($,.STERADIAN.)
SOLID_ANGLE_UNIT()
);
#63037=SHAPE_DEFINITION_REPRESENTATION(#63168,#63397);
#63168=PRODUCT_DEFINITION_SHAPE('',$,#63496);
#63397=SHAPE_REPRESENTATION('',(#25118),#62934);
#63447=PRODUCT_DEFINITION_CONTEXT('part definition',#63743,'design');
#63496=PRODUCT_DEFINITION('Flat Washer - M6','Flat Washer - M6',#63594,
#63447);
#63594=PRODUCT_DEFINITION_FORMATION('',$,#63793);
#63743=APPLICATION_CONTEXT(
'Core Data for Automotive Mechanical Design Process');
#63744=PRODUCT_CONTEXT('part definition',#63743,'mechanical');
#63793=PRODUCT('Flat Washer - M6','Flat Washer - M6','Flat Washer - M6',
(#63744));
#63913=COLOUR_RGB('Black',0.12,0.14,0.17);
#63914=FILL_AREA_STYLE_COLOUR('',#63913);
#63915=FILL_AREA_STYLE('',(#63914));
#63916=SURFACE_STYLE_FILL_AREA(#63915);
#63917=SURFACE_SIDE_STYLE('',(#63916));
#63918=SURFACE_STYLE_USAGE(.BOTH.,#63917);
#63919=PRESENTATION_STYLE_ASSIGNMENT((#63918));
ENDSEC;
END-ISO-10303-21;
